ISO-10303-21;
HEADER;
/* Generated by software containing ST-Developer
 * from STEP Tools, Inc. (www.steptools.com) 
 */

FILE_DESCRIPTION(
/* description */ ('PAT-091'),
/* implementation_level */ '2;1');

FILE_NAME(
/* name */ 'Lower nut carriage.step',
/* time_stamp */ '2026-10-27T15:34:44-07:00',
/* author */ (''),
/* organization */ (''),
/* preprocessor_version */ 'ST-DEVELOPER v20.2',
/* originating_system */ 'Autodesk Translation Framework v15.17.0.0',
/* authorisation */ '');

FILE_SCHEMA (('AUTOMOTIVE_DESIGN { 1 0 10303 214 3 1 1 }'));
ENDSEC;

DATA;
#10=MECHANICAL_DESIGN_GEOMETRIC_PRESENTATION_REPRESENTATION('',(#1002),#25100);
#782=SHAPE_REPRESENTATION_RELATIONSHIP('SRR','None',#25545,#892);
#892=ADVANCED_BREP_SHAPE_REPRESENTATION('',(#1124),#25015);
#1002=STYLED_ITEM('',(#26198),#1124);
#1124=MANIFOLD_SOLID_BREP('Body1',#13281);
#1392=FACE_BOUND('',#3323,.T.);
#1393=FACE_BOUND('',#3324,.T.);
#1394=FACE_BOUND('',#3325,.T.);
#1395=FACE_BOUND('',#3328,.T.);
#1396=FACE_BOUND('',#3329,.T.);
#1397=FACE_BOUND('',#3330,.T.);
#1777=PLANE('',#15129);
#1778=PLANE('',#15130);
#1779=PLANE('',#15131);
#1780=PLANE('',#15132);
#1781=PLANE('',#15133);
#1782=PLANE('',#15134);
#2323=FACE_OUTER_BOUND('',#3318,.T.);
#2324=FACE_OUTER_BOUND('',#3319,.T.);
#2325=FACE_OUTER_BOUND('',#3320,.T.);
#2326=FACE_OUTER_BOUND('',#3321,.T.);
#2327=FACE_OUTER_BOUND('',#3322,.T.);
#2328=FACE_OUTER_BOUND('',#3326,.T.);
#2329=FACE_OUTER_BOUND('',#3327,.T.);
#2330=FACE_OUTER_BOUND('',#3331,.T.);
#2331=FACE_OUTER_BOUND('',#3332,.T.);
#3318=EDGE_LOOP('',(#10056,#10057,#10058,#10059));
#3319=EDGE_LOOP('',(#10060,#10061,#10062,#10063));
#3320=EDGE_LOOP('',(#10064,#10065,#10066,#10067));
#3321=EDGE_LOOP('',(#10068,#10069,#10070,#10071));
#3322=EDGE_LOOP('',(#10072,#10073,#10074,#10075));
#3323=EDGE_LOOP('',(#10076));
#3324=EDGE_LOOP('',(#10077));
#3325=EDGE_LOOP('',(#10078));
#3326=EDGE_LOOP('',(#10079,#10080,#10081,#10082));
#3327=EDGE_LOOP('',(#10083,#10084,#10085,#10086));
#3328=EDGE_LOOP('',(#10087));
#3329=EDGE_LOOP('',(#10088));
#3330=EDGE_LOOP('',(#10089));
#3331=EDGE_LOOP('',(#10090,#10091,#10092,#10093));
#3332=EDGE_LOOP('',(#10094,#10095,#10096,#10097));
#4427=LINE('',#22175,#5167);
#4428=LINE('',#22181,#5168);
#4429=LINE('',#22187,#5169);
#4430=LINE('',#22192,#5170);
#4431=LINE('',#22194,#5171);
#4432=LINE('',#22196,#5172);
#4433=LINE('',#22197,#5173);
#4434=LINE('',#22200,#5174);
#4435=LINE('',#22202,#5175);
#4436=LINE('',#22203,#5176);
#4437=LINE('',#22206,#5177);
#4438=LINE('',#22208,#5178);
#4439=LINE('',#22209,#5179);
#4440=LINE('',#22211,#5180);
#4441=LINE('',#22212,#5181);
#5167=VECTOR('',#17845,0.5);
#5168=VECTOR('',#17852,1.05);
#5169=VECTOR('',#17859,1.05);
#5170=VECTOR('',#17864,1.);
#5171=VECTOR('',#17865,1.);
#5172=VECTOR('',#17866,1.);
#5173=VECTOR('',#17867,1.);
#5174=VECTOR('',#17870,1.);
#5175=VECTOR('',#17871,1.);
#5176=VECTOR('',#17872,1.);
#5177=VECTOR('',#17875,1.);
#5178=VECTOR('',#17876,1.);
#5179=VECTOR('',#17877,1.);
#5180=VECTOR('',#17880,1.);
#5181=VECTOR('',#17881,1.);
#5843=CIRCLE('',#15121,0.5);
#5844=CIRCLE('',#15122,0.5);
#5845=CIRCLE('',#15124,1.05);
#5846=CIRCLE('',#15125,1.05);
#5847=CIRCLE('',#15127,1.05);
#5848=CIRCLE('',#15128,1.05);
#6742=VERTEX_POINT('',#22172);
#6743=VERTEX_POINT('',#22174);
#6744=VERTEX_POINT('',#22178);
#6745=VERTEX_POINT('',#22180);
#6746=VERTEX_POINT('',#22184);
#6747=VERTEX_POINT('',#22186);
#6748=VERTEX_POINT('',#22190);
#6749=VERTEX_POINT('',#22191);
#6750=VERTEX_POINT('',#22193);
#6751=VERTEX_POINT('',#22195);
#6752=VERTEX_POINT('',#22199);
#6753=VERTEX_POINT('',#22201);
#6754=VERTEX_POINT('',#22205);
#6755=VERTEX_POINT('',#22207);
#7963=EDGE_CURVE('',#6742,#6742,#5843,.T.);
#7964=EDGE_CURVE('',#6742,#6743,#4427,.T.);
#7965=EDGE_CURVE('',#6743,#6743,#5844,.T.);
#7966=EDGE_CURVE('',#6744,#6744,#5845,.T.);
#7967=EDGE_CURVE('',#6744,#6745,#4428,.T.);
#7968=EDGE_CURVE('',#6745,#6745,#5846,.T.);
#7969=EDGE_CURVE('',#6746,#6746,#5847,.T.);
#7970=EDGE_CURVE('',#6746,#6747,#4429,.T.);
#7971=EDGE_CURVE('',#6747,#6747,#5848,.T.);
#7972=EDGE_CURVE('',#6748,#6749,#4430,.T.);
#7973=EDGE_CURVE('',#6749,#6750,#4431,.T.);
#7974=EDGE_CURVE('',#6751,#6750,#4432,.T.);
#7975=EDGE_CURVE('',#6748,#6751,#4433,.T.);
#7976=EDGE_CURVE('',#6752,#6748,#4434,.T.);
#7977=EDGE_CURVE('',#6753,#6751,#4435,.T.);
#7978=EDGE_CURVE('',#6752,#6753,#4436,.T.);
#7979=EDGE_CURVE('',#6754,#6752,#4437,.T.);
#7980=EDGE_CURVE('',#6755,#6753,#4438,.T.);
#7981=EDGE_CURVE('',#6754,#6755,#4439,.T.);
#7982=EDGE_CURVE('',#6749,#6754,#4440,.T.);
#7983=EDGE_CURVE('',#6750,#6755,#4441,.T.);
#10056=ORIENTED_EDGE('',*,*,#7963,.F.);
#10057=ORIENTED_EDGE('',*,*,#7964,.T.);
#10058=ORIENTED_EDGE('',*,*,#7965,.F.);
#10059=ORIENTED_EDGE('',*,*,#7964,.F.);
#10060=ORIENTED_EDGE('',*,*,#7966,.F.);
#10061=ORIENTED_EDGE('',*,*,#7967,.T.);
#10062=ORIENTED_EDGE('',*,*,#7968,.F.);
#10063=ORIENTED_EDGE('',*,*,#7967,.F.);
#10064=ORIENTED_EDGE('',*,*,#7969,.F.);
#10065=ORIENTED_EDGE('',*,*,#7970,.T.);
#10066=ORIENTED_EDGE('',*,*,#7971,.F.);
#10067=ORIENTED_EDGE('',*,*,#7970,.F.);
#10068=ORIENTED_EDGE('',*,*,#7972,.T.);
#10069=ORIENTED_EDGE('',*,*,#7973,.T.);
#10070=ORIENTED_EDGE('',*,*,#7974,.F.);
#10071=ORIENTED_EDGE('',*,*,#7975,.F.);
#10072=ORIENTED_EDGE('',*,*,#7976,.T.);
#10073=ORIENTED_EDGE('',*,*,#7975,.T.);
#10074=ORIENTED_EDGE('',*,*,#7977,.F.);
#10075=ORIENTED_EDGE('',*,*,#7978,.F.);
#10076=ORIENTED_EDGE('',*,*,#7965,.T.);
#10077=ORIENTED_EDGE('',*,*,#7968,.T.);
#10078=ORIENTED_EDGE('',*,*,#7971,.T.);
#10079=ORIENTED_EDGE('',*,*,#7979,.T.);
#10080=ORIENTED_EDGE('',*,*,#7978,.T.);
#10081=ORIENTED_EDGE('',*,*,#7980,.F.);
#10082=ORIENTED_EDGE('',*,*,#7981,.F.);
#10083=ORIENTED_EDGE('',*,*,#7982,.T.);
#10084=ORIENTED_EDGE('',*,*,#7981,.T.);
#10085=ORIENTED_EDGE('',*,*,#7983,.F.);
#10086=ORIENTED_EDGE('',*,*,#7973,.F.);
#10087=ORIENTED_EDGE('',*,*,#7963,.T.);
#10088=ORIENTED_EDGE('',*,*,#7966,.T.);
#10089=ORIENTED_EDGE('',*,*,#7969,.T.);
#10090=ORIENTED_EDGE('',*,*,#7983,.T.);
#10091=ORIENTED_EDGE('',*,*,#7980,.T.);
#10092=ORIENTED_EDGE('',*,*,#7977,.T.);
#10093=ORIENTED_EDGE('',*,*,#7974,.T.);
#10094=ORIENTED_EDGE('',*,*,#7982,.F.);
#10095=ORIENTED_EDGE('',*,*,#7972,.F.);
#10096=ORIENTED_EDGE('',*,*,#7976,.F.);
#10097=ORIENTED_EDGE('',*,*,#7979,.F.);
#12190=CYLINDRICAL_SURFACE('',#15120,0.5);
#12191=CYLINDRICAL_SURFACE('',#15123,1.05);
#12192=CYLINDRICAL_SURFACE('',#15126,1.05);
#12690=ADVANCED_FACE('',(#2323),#12190,.F.);
#12691=ADVANCED_FACE('',(#2324),#12191,.F.);
#12692=ADVANCED_FACE('',(#2325),#12192,.F.);
#12693=ADVANCED_FACE('',(#2326),#1777,.T.);
#12694=ADVANCED_FACE('',(#2327,#1392,#1393,#1394),#1778,.T.);
#12695=ADVANCED_FACE('',(#2328),#1779,.T.);
#12696=ADVANCED_FACE('',(#2329,#1395,#1396,#1397),#1780,.T.);
#12697=ADVANCED_FACE('',(#2330),#1781,.T.);
#12698=ADVANCED_FACE('',(#2331),#1782,.F.);
#13281=CLOSED_SHELL('',(#12690,#12691,#12692,#12693,#12694,#12695,#12696,
#12697,#12698));
#15119=AXIS2_PLACEMENT_3D('',#22170,#17839,#17840);
#15120=AXIS2_PLACEMENT_3D('',#22171,#17841,#17842);
#15121=AXIS2_PLACEMENT_3D('',#22173,#17843,#17844);
#15122=AXIS2_PLACEMENT_3D('',#22176,#17846,#17847);
#15123=AXIS2_PLACEMENT_3D('',#22177,#17848,#17849);
#15124=AXIS2_PLACEMENT_3D('',#22179,#17850,#17851);
#15125=AXIS2_PLACEMENT_3D('',#22182,#17853,#17854);
#15126=AXIS2_PLACEMENT_3D('',#22183,#17855,#17856);
#15127=AXIS2_PLACEMENT_3D('',#22185,#17857,#17858);
#15128=AXIS2_PLACEMENT_3D('',#22188,#17860,#17861);
#15129=AXIS2_PLACEMENT_3D('',#22189,#17862,#17863);
#15130=AXIS2_PLACEMENT_3D('',#22198,#17868,#17869);
#15131=AXIS2_PLACEMENT_3D('',#22204,#17873,#17874);
#15132=AXIS2_PLACEMENT_3D('',#22210,#17878,#17879);
#15133=AXIS2_PLACEMENT_3D('',#22213,#17882,#17883);
#15134=AXIS2_PLACEMENT_3D('',#22214,#17884,#17885);
#17839=DIRECTION('axis',(0.,0.,1.));
#17840=DIRECTION('refdir',(1.,0.,0.));
#17841=DIRECTION('center_axis',(1.,0.,0.));
#17842=DIRECTION('ref_axis',(0.,0.,-1.));
#17843=DIRECTION('center_axis',(1.,0.,0.));
#17844=DIRECTION('ref_axis',(0.,0.,-1.));
#17845=DIRECTION('',(1.,0.,0.));
#17846=DIRECTION('center_axis',(-1.,0.,0.));
#17847=DIRECTION('ref_axis',(0.,0.,-1.));
#17848=DIRECTION('center_axis',(1.,0.,0.));
#17849=DIRECTION('ref_axis',(0.,0.,-1.));
#17850=DIRECTION('center_axis',(1.,0.,0.));
#17851=DIRECTION('ref_axis',(0.,0.,-1.));
#17852=DIRECTION('',(1.,0.,0.));
#17853=DIRECTION('center_axis',(-1.,0.,0.));
#17854=DIRECTION('ref_axis',(0.,0.,-1.));
#17855=DIRECTION('center_axis',(1.,0.,0.));
#17856=DIRECTION('ref_axis',(0.,0.,-1.));
#17857=DIRECTION('center_axis',(1.,0.,0.));
#17858=DIRECTION('ref_axis',(0.,0.,-1.));
#17859=DIRECTION('',(1.,0.,0.));
#17860=DIRECTION('center_axis',(-1.,0.,0.));
#17861=DIRECTION('ref_axis',(0.,0.,-1.));
#17862=DIRECTION('center_axis',(0.,1.,0.));
#17863=DIRECTION('ref_axis',(-1.,0.,0.));
#17864=DIRECTION('',(-1.,0.,0.));
#17865=DIRECTION('',(0.,0.,1.));
#17866=DIRECTION('',(-1.,0.,0.));
#17867=DIRECTION('',(0.,0.,1.));
#17868=DIRECTION('center_axis',(1.,0.,0.));
#17869=DIRECTION('ref_axis',(0.,1.,0.));
#17870=DIRECTION('',(0.,1.,0.));
#17871=DIRECTION('',(0.,1.,0.));
#17872=DIRECTION('',(0.,0.,1.));
#17873=DIRECTION('center_axis',(0.,-1.,0.));
#17874=DIRECTION('ref_axis',(1.,0.,0.));
#17875=DIRECTION('',(1.,0.,0.));
#17876=DIRECTION('',(1.,0.,0.));
#17877=DIRECTION('',(0.,0.,1.));
#17878=DIRECTION('center_axis',(-1.,0.,0.));
#17879=DIRECTION('ref_axis',(0.,-1.,0.));
#17880=DIRECTION('',(0.,-1.,0.));
#17881=DIRECTION('',(0.,-1.,0.));
#17882=DIRECTION('center_axis',(0.,0.,1.));
#17883=DIRECTION('ref_axis',(1.,0.,0.));
#17884=DIRECTION('center_axis',(0.,0.,1.));
#17885=DIRECTION('ref_axis',(1.,0.,0.));
#22170=CARTESIAN_POINT('',(0.,0.,0.));
#22171=CARTESIAN_POINT('Origin',(36.92983346,0.,6.));
#22172=CARTESIAN_POINT('',(37.0298334620742,-6.12323399573677E-17,6.5));
#22173=CARTESIAN_POINT('Origin',(37.0298334620742,0.,6.));
#22174=CARTESIAN_POINT('',(40.4298334620742,6.12323399573677E-17,6.5));
#22175=CARTESIAN_POINT('',(36.92983346,-6.12323399573677E-17,6.5));
#22176=CARTESIAN_POINT('Origin',(40.4298334620742,0.,6.));
#22177=CARTESIAN_POINT('Origin',(36.92983346,-3.,6.));
#22178=CARTESIAN_POINT('',(37.0298334620742,-3.,7.05));
#22179=CARTESIAN_POINT('Origin',(37.0298334620742,-3.,6.));
#22180=CARTESIAN_POINT('',(40.4298334620742,-3.,7.05));
#22181=CARTESIAN_POINT('',(36.92983346,-3.,7.05));
#22182=CARTESIAN_POINT('Origin',(40.4298334620742,-3.,6.));
#22183=CARTESIAN_POINT('Origin',(36.92983346,3.,6.));
#22184=CARTESIAN_POINT('',(37.0298334620742,3.,7.05));
#22185=CARTESIAN_POINT('Origin',(37.0298334620742,3.,6.));
#22186=CARTESIAN_POINT('',(40.4298334620742,3.,7.05));
#22187=CARTESIAN_POINT('',(36.92983346,3.,7.05));
#22188=CARTESIAN_POINT('Origin',(40.4298334620742,3.,6.));
#22189=CARTESIAN_POINT('Origin',(40.4298334620742,4.7,4.3));
#22190=CARTESIAN_POINT('',(40.4298334620742,4.7,4.3));
#22191=CARTESIAN_POINT('',(37.0298334620742,4.7,4.3));
#22192=CARTESIAN_POINT('',(40.4298334620742,4.7,4.3));
#22193=CARTESIAN_POINT('',(37.0298334620742,4.7,7.7));
#22194=CARTESIAN_POINT('',(37.0298334620742,4.7,4.3));
#22195=CARTESIAN_POINT('',(40.4298334620742,4.7,7.7));
#22196=CARTESIAN_POINT('',(40.4298334620742,4.7,7.7));
#22197=CARTESIAN_POINT('',(40.4298334620742,4.7,4.3));
#22198=CARTESIAN_POINT('Origin',(40.4298334620742,-4.3,4.3));
#22199=CARTESIAN_POINT('',(40.4298334620742,-4.3,4.3));
#22200=CARTESIAN_POINT('',(40.4298334620742,-4.3,4.3));
#22201=CARTESIAN_POINT('',(40.4298334620742,-4.3,7.7));
#22202=CARTESIAN_POINT('',(40.4298334620742,-4.3,7.7));
#22203=CARTESIAN_POINT('',(40.4298334620742,-4.3,4.3));
#22204=CARTESIAN_POINT('Origin',(37.0298334620742,-4.3,4.3));
#22205=CARTESIAN_POINT('',(37.0298334620742,-4.3,4.3));
#22206=CARTESIAN_POINT('',(37.0298334620742,-4.3,4.3));
#22207=CARTESIAN_POINT('',(37.0298334620742,-4.3,7.7));
#22208=CARTESIAN_POINT('',(37.0298334620742,-4.3,7.7));
#22209=CARTESIAN_POINT('',(37.0298334620742,-4.3,4.3));
#22210=CARTESIAN_POINT('Origin',(37.0298334620742,4.7,4.3));
#22211=CARTESIAN_POINT('',(37.0298334620742,4.7,4.3));
#22212=CARTESIAN_POINT('',(37.0298334620742,4.7,7.7));
#22213=CARTESIAN_POINT('Origin',(38.7298334620742,0.2,7.7));
#22214=CARTESIAN_POINT('Origin',(38.7298334620742,0.2,4.3));
#24894=UNCERTAINTY_MEASURE_WITH_UNIT(LENGTH_MEASURE(0.001),#25101,
'DISTANCE_ACCURACY_VALUE',
'Maximum model space distance between geometric entities at asserted c
onnectivities');
#24979=UNCERTAINTY_MEASURE_WITH_UNIT(LENGTH_MEASURE(0.001),#25101,
'DISTANCE_ACCURACY_VALUE',
'Maximum model space distance between geometric entities at asserted c
onnectivities');
#25015=(
GEOMETRIC_REPRESENTATION_CONTEXT(3)
GLOBAL_UNCERTAINTY_ASSIGNED_CONTEXT((#24894))
GLOBAL_UNIT_ASSIGNED_CONTEXT((#25101,#25103,#25104))
REPRESENTATION_CONTEXT('','3D')
);
#25100=(
GEOMETRIC_REPRESENTATION_CONTEXT(3)
GLOBAL_UNCERTAINTY_ASSIGNED_CONTEXT((#24979))
GLOBAL_UNIT_ASSIGNED_CONTEXT((#25101,#25103,#25104))
REPRESENTATION_CONTEXT('','3D')
);
#25101=(
LENGTH_UNIT()
NAMED_UNIT(*)
SI_UNIT(.CENTI.,.METRE.)
);
#25103=(
NAMED_UNIT(*)
PLANE_ANGLE_UNIT()
SI_UNIT($,.RADIAN.)
);
#25104=(
NAMED_UNIT(*)
SI_UNIT($,.STERADIAN.)
SOLID_ANGLE_UNIT()
);
#25140=SHAPE_DEFINITION_REPRESENTATION(#25260,#25545);
#25260=PRODUCT_DEFINITION_SHAPE('',$,#25666);
#25545=SHAPE_REPRESENTATION('',(#15119),#25015);
#25630=PRODUCT_DEFINITION_CONTEXT('part definition',#25992,'design');
#25666=PRODUCT_DEFINITION('Lower nut carriage','Lower nut carriage',#25786,
#25630);
#25786=PRODUCT_DEFINITION_FORMATION('',$,#26029);
#25992=APPLICATION_CONTEXT(
'Core Data for Automotive Mechanical Design Process');
#25993=PRODUCT_CONTEXT('part definition',#25992,'mechanical');
#26029=PRODUCT('Lower nut carriage','Lower nut carriage',
'Lower nut carriage',(#25993));
#26192=COLOUR_RGB('Black',0.12,0.14,0.17);
#26193=FILL_AREA_STYLE_COLOUR('',#26192);
#26194=FILL_AREA_STYLE('',(#26193));
#26195=SURFACE_STYLE_FILL_AREA(#26194);
#26196=SURFACE_SIDE_STYLE('',(#26195));
#26197=SURFACE_STYLE_USAGE(.BOTH.,#26196);
#26198=PRESENTATION_STYLE_ASSIGNMENT((#26197));
ENDSEC;
END-ISO-10303-21;
